ISO-10303-21;
HEADER;
/* Generated by software containing ST-Developer
 * from STEP Tools, Inc. (www.steptools.com) 
 */

FILE_DESCRIPTION(
/* description */ ('Bin tilter linkage'),
/* implementation_level */ '2;1');

FILE_NAME(
/* name */ 'M4 short cap screw (31).step',
/* time_stamp */ '2026-10-28T03:26:24-07:00',
/* author */ (''),
/* organization */ (''),
/* preprocessor_version */ 'ST-DEVELOPER v20.2',
/* originating_system */ 'Autodesk Translation Framework v15.17.0.0',
/* authorisation */ '');

FILE_SCHEMA (('AUTOMOTIVE_DESIGN { 1 0 10303 214 3 1 1 }'));
ENDSEC;

DATA;
#10=MECHANICAL_DESIGN_GEOMETRIC_PRESENTATION_REPRESENTATION('',(#933),#23728);
#721=SHAPE_REPRESENTATION_RELATIONSHIP('SRR','None',#24187,#827);
#827=ADVANCED_BREP_SHAPE_REPRESENTATION('',(#1046),#23687);
#933=STYLED_ITEM('',(#24772),#1046);
#1046=MANIFOLD_SOLID_BREP('Body1',#12464);
#1385=FACE_BOUND('',#3466,.T.);
#1734=PLANE('',#14764);
#1735=PLANE('',#14769);
#1736=PLANE('',#14772);
#2390=FACE_OUTER_BOUND('',#3465,.T.);
#2391=FACE_OUTER_BOUND('',#3467,.T.);
#2392=FACE_OUTER_BOUND('',#3468,.T.);
#2393=FACE_OUTER_BOUND('',#3469,.T.);
#2394=FACE_OUTER_BOUND('',#3470,.T.);
#3465=EDGE_LOOP('',(#10201));
#3466=EDGE_LOOP('',(#10202));
#3467=EDGE_LOOP('',(#10203,#10204,#10205,#10206));
#3468=EDGE_LOOP('',(#10207));
#3469=EDGE_LOOP('',(#10208,#10209,#10210,#10211));
#3470=EDGE_LOOP('',(#10212));
#4251=LINE('',#21851,#4926);
#4252=LINE('',#21855,#4927);
#4926=VECTOR('',#18062,0.350000000000001);
#4927=VECTOR('',#18067,0.199999999999999);
#5711=CIRCLE('',#14765,0.350000000000001);
#5712=CIRCLE('',#14766,0.199999999999999);
#5713=CIRCLE('',#14768,0.350000000000001);
#5714=CIRCLE('',#14771,0.199999999999999);
#6565=VERTEX_POINT('',#21844);
#6566=VERTEX_POINT('',#21846);
#6567=VERTEX_POINT('',#21849);
#6568=VERTEX_POINT('',#21854);
#7840=EDGE_CURVE('',#6565,#6565,#5711,.T.);
#7841=EDGE_CURVE('',#6566,#6566,#5712,.T.);
#7842=EDGE_CURVE('',#6567,#6567,#5713,.T.);
#7843=EDGE_CURVE('',#6567,#6565,#4251,.T.);
#7844=EDGE_CURVE('',#6566,#6568,#4252,.T.);
#7845=EDGE_CURVE('',#6568,#6568,#5714,.T.);
#10201=ORIENTED_EDGE('',*,*,#7840,.F.);
#10202=ORIENTED_EDGE('',*,*,#7841,.T.);
#10203=ORIENTED_EDGE('',*,*,#7842,.F.);
#10204=ORIENTED_EDGE('',*,*,#7843,.T.);
#10205=ORIENTED_EDGE('',*,*,#7840,.T.);
#10206=ORIENTED_EDGE('',*,*,#7843,.F.);
#10207=ORIENTED_EDGE('',*,*,#7842,.T.);
#10208=ORIENTED_EDGE('',*,*,#7841,.F.);
#10209=ORIENTED_EDGE('',*,*,#7844,.T.);
#10210=ORIENTED_EDGE('',*,*,#7845,.T.);
#10211=ORIENTED_EDGE('',*,*,#7844,.F.);
#10212=ORIENTED_EDGE('',*,*,#7845,.F.);
#11521=CYLINDRICAL_SURFACE('',#14767,0.350000000000001);
#11522=CYLINDRICAL_SURFACE('',#14770,0.199999999999999);
#12115=ADVANCED_FACE('',(#2390,#1385),#1734,.F.);
#12116=ADVANCED_FACE('',(#2391),#11521,.T.);
#12117=ADVANCED_FACE('',(#2392),#1735,.T.);
#12118=ADVANCED_FACE('',(#2393),#11522,.T.);
#12119=ADVANCED_FACE('',(#2394),#1736,.F.);
#12464=CLOSED_SHELL('',(#12115,#12116,#12117,#12118,#12119));
#14763=AXIS2_PLACEMENT_3D('',#21842,#18050,#18051);
#14764=AXIS2_PLACEMENT_3D('',#21843,#18052,#18053);
#14765=AXIS2_PLACEMENT_3D('',#21845,#18054,#18055);
#14766=AXIS2_PLACEMENT_3D('',#21847,#18056,#18057);
#14767=AXIS2_PLACEMENT_3D('',#21848,#18058,#18059);
#14768=AXIS2_PLACEMENT_3D('',#21850,#18060,#18061);
#14769=AXIS2_PLACEMENT_3D('',#21852,#18063,#18064);
#14770=AXIS2_PLACEMENT_3D('',#21853,#18065,#18066);
#14771=AXIS2_PLACEMENT_3D('',#21856,#18068,#18069);
#14772=AXIS2_PLACEMENT_3D('',#21857,#18070,#18071);
#18050=DIRECTION('axis',(0.,0.,1.));
#18051=DIRECTION('refdir',(1.,0.,0.));
#18052=DIRECTION('center_axis',(0.,1.,0.));
#18053=DIRECTION('ref_axis',(1.,0.,0.));
#18054=DIRECTION('center_axis',(0.,1.,0.));
#18055=DIRECTION('ref_axis',(1.,0.,0.));
#18056=DIRECTION('center_axis',(0.,1.,0.));
#18057=DIRECTION('ref_axis',(1.,0.,0.));
#18058=DIRECTION('center_axis',(0.,1.,0.));
#18059=DIRECTION('ref_axis',(1.,0.,0.));
#18060=DIRECTION('center_axis',(0.,1.,0.));
#18061=DIRECTION('ref_axis',(1.,0.,0.));
#18062=DIRECTION('',(0.,-1.,0.));
#18063=DIRECTION('center_axis',(0.,1.,0.));
#18064=DIRECTION('ref_axis',(1.,0.,0.));
#18065=DIRECTION('center_axis',(0.,1.,0.));
#18066=DIRECTION('ref_axis',(1.,0.,0.));
#18067=DIRECTION('',(0.,-1.,0.));
#18068=DIRECTION('center_axis',(0.,1.,0.));
#18069=DIRECTION('ref_axis',(1.,0.,0.));
#18070=DIRECTION('center_axis',(0.,1.,0.));
#18071=DIRECTION('ref_axis',(1.,0.,0.));
#21842=CARTESIAN_POINT('',(0.,0.,0.));
#21843=CARTESIAN_POINT('Origin',(25.5102260242172,0.8,27.3496056572921));
#21844=CARTESIAN_POINT('',(25.1602260242172,0.8,27.3496056572921));
#21845=CARTESIAN_POINT('Origin',(25.5102260242172,0.8,27.3496056572921));
#21846=CARTESIAN_POINT('',(25.3102260242172,0.8,27.3496056572921));
#21847=CARTESIAN_POINT('Origin',(25.5102260242172,0.8,27.3496056572921));
#21848=CARTESIAN_POINT('Origin',(25.5102260242172,0.8,27.3496056572921));
#21849=CARTESIAN_POINT('',(25.1602260242172,1.2,27.3496056572921));
#21850=CARTESIAN_POINT('Origin',(25.5102260242172,1.2,27.3496056572921));
#21851=CARTESIAN_POINT('',(25.1602260242172,0.8,27.3496056572921));
#21852=CARTESIAN_POINT('Origin',(25.5102260242172,1.2,27.3496056572921));
#21853=CARTESIAN_POINT('Origin',(25.5102260242172,0.1,27.3496056572921));
#21854=CARTESIAN_POINT('',(25.3102260242172,0.1,27.3496056572921));
#21855=CARTESIAN_POINT('',(25.3102260242172,0.1,27.3496056572921));
#21856=CARTESIAN_POINT('Origin',(25.5102260242172,0.1,27.3496056572921));
#21857=CARTESIAN_POINT('Origin',(25.5102260242172,0.1,27.3496056572921));
#23570=UNCERTAINTY_MEASURE_WITH_UNIT(LENGTH_MEASURE(0.001),#23729,
'DISTANCE_ACCURACY_VALUE',
'Maximum model space distance between geometric entities at asserted c
onnectivities');
#23611=UNCERTAINTY_MEASURE_WITH_UNIT(LENGTH_MEASURE(0.001),#23729,
'DISTANCE_ACCURACY_VALUE',
'Maximum model space distance between geometric entities at asserted c
onnectivities');
#23687=(
GEOMETRIC_REPRESENTATION_CONTEXT(3)
GLOBAL_UNCERTAINTY_ASSIGNED_CONTEXT((#23570))
GLOBAL_UNIT_ASSIGNED_CONTEXT((#23729,#23731,#23732))
REPRESENTATION_CONTEXT('','3D')
);
#23728=(
GEOMETRIC_REPRESENTATION_CONTEXT(3)
GLOBAL_UNCERTAINTY_ASSIGNED_CONTEXT((#23611))
GLOBAL_UNIT_ASSIGNED_CONTEXT((#23729,#23731,#23732))
REPRESENTATION_CONTEXT('','3D')
);
#23729=(
LENGTH_UNIT()
NAMED_UNIT(*)
SI_UNIT(.CENTI.,.METRE.)
);
#23731=(
NAMED_UNIT(*)
PLANE_ANGLE_UNIT()
SI_UNIT($,.RADIAN.)
);
#23732=(
NAMED_UNIT(*)
SI_UNIT($,.STERADIAN.)
SOLID_ANGLE_UNIT()
);
#23808=SHAPE_DEFINITION_REPRESENTATION(#23924,#24187);
#23924=PRODUCT_DEFINITION_SHAPE('',$,#24304);
#24187=SHAPE_REPRESENTATION('',(#14763),#23687);
#24228=PRODUCT_DEFINITION_CONTEXT('part definition',#24578,'design');
#24304=PRODUCT_DEFINITION('M4 short cap screw (31)',
'M4 short cap screw (31)',#24420,#24228);
#24420=PRODUCT_DEFINITION_FORMATION('',$,#24655);
#24578=APPLICATION_CONTEXT(
'Core Data for Automotive Mechanical Design Process');
#24579=PRODUCT_CONTEXT('part definition',#24578,'mechanical');
#24655=PRODUCT('M4 short cap screw (31)','M4 short cap screw (31)',
'M4 short cap screw (31)',(#24579));
#24766=COLOUR_RGB('Black',0.12,0.14,0.17);
#24767=FILL_AREA_STYLE_COLOUR('',#24766);
#24768=FILL_AREA_STYLE('',(#24767));
#24769=SURFACE_STYLE_FILL_AREA(#24768);
#24770=SURFACE_SIDE_STYLE('',(#24769));
#24771=SURFACE_STYLE_USAGE(.BOTH.,#24770);
#24772=PRESENTATION_STYLE_ASSIGNMENT((#24771));
ENDSEC;
END-ISO-10303-21;
